ISO-10303-21;
HEADER;
/* Generated by software containing ST-Developer
 * from STEP Tools, Inc. (www.steptools.com) 
 */

FILE_DESCRIPTION(
/* description */ ('Bin tilter linkage'),
/* implementation_level */ '2;1');

FILE_NAME(
/* name */ 'M4 short cap screw (23).step',
/* time_stamp */ '2026-10-28T03:26:24-07:00',
/* author */ (''),
/* organization */ (''),
/* preprocessor_version */ 'ST-DEVELOPER v20.2',
/* originating_system */ 'Autodesk Translation Framework v15.17.0.0',
/* authorisation */ '');

FILE_SCHEMA (('AUTOMOTIVE_DESIGN { 1 0 10303 214 3 1 1 }'));
ENDSEC;

DATA;
#10=MECHANICAL_DESIGN_GEOMETRIC_PRESENTATION_REPRESENTATION('',(#923),#23728);
#711=SHAPE_REPRESENTATION_RELATIONSHIP('SRR','None',#24177,#817);
#817=ADVANCED_BREP_SHAPE_REPRESENTATION('',(#1036),#23677);
#923=STYLED_ITEM('',(#24772),#1036);
#1036=MANIFOLD_SOLID_BREP('Body1',#12454);
#1357=FACE_BOUND('',#3382,.T.);
#1706=PLANE('',#14642);
#1707=PLANE('',#14647);
#1708=PLANE('',#14650);
#2334=FACE_OUTER_BOUND('',#3381,.T.);
#2335=FACE_OUTER_BOUND('',#3383,.T.);
#2336=FACE_OUTER_BOUND('',#3384,.T.);
#2337=FACE_OUTER_BOUND('',#3385,.T.);
#2338=FACE_OUTER_BOUND('',#3386,.T.);
#3381=EDGE_LOOP('',(#10033));
#3382=EDGE_LOOP('',(#10034));
#3383=EDGE_LOOP('',(#10035,#10036,#10037,#10038));
#3384=EDGE_LOOP('',(#10039));
#3385=EDGE_LOOP('',(#10040,#10041,#10042,#10043));
#3386=EDGE_LOOP('',(#10044));
#4223=LINE('',#21645,#4898);
#4224=LINE('',#21649,#4899);
#4898=VECTOR('',#17790,0.350000000000001);
#4899=VECTOR('',#17795,0.199999999999999);
#5655=CIRCLE('',#14643,0.350000000000001);
#5656=CIRCLE('',#14644,0.199999999999999);
#5657=CIRCLE('',#14646,0.350000000000001);
#5658=CIRCLE('',#14649,0.199999999999999);
#6509=VERTEX_POINT('',#21638);
#6510=VERTEX_POINT('',#21640);
#6511=VERTEX_POINT('',#21643);
#6512=VERTEX_POINT('',#21648);
#7756=EDGE_CURVE('',#6509,#6509,#5655,.T.);
#7757=EDGE_CURVE('',#6510,#6510,#5656,.T.);
#7758=EDGE_CURVE('',#6511,#6511,#5657,.T.);
#7759=EDGE_CURVE('',#6511,#6509,#4223,.T.);
#7760=EDGE_CURVE('',#6510,#6512,#4224,.T.);
#7761=EDGE_CURVE('',#6512,#6512,#5658,.T.);
#10033=ORIENTED_EDGE('',*,*,#7756,.F.);
#10034=ORIENTED_EDGE('',*,*,#7757,.T.);
#10035=ORIENTED_EDGE('',*,*,#7758,.F.);
#10036=ORIENTED_EDGE('',*,*,#7759,.T.);
#10037=ORIENTED_EDGE('',*,*,#7756,.T.);
#10038=ORIENTED_EDGE('',*,*,#7759,.F.);
#10039=ORIENTED_EDGE('',*,*,#7758,.T.);
#10040=ORIENTED_EDGE('',*,*,#7757,.F.);
#10041=ORIENTED_EDGE('',*,*,#7760,.T.);
#10042=ORIENTED_EDGE('',*,*,#7761,.T.);
#10043=ORIENTED_EDGE('',*,*,#7760,.F.);
#10044=ORIENTED_EDGE('',*,*,#7761,.F.);
#11493=CYLINDRICAL_SURFACE('',#14645,0.350000000000001);
#11494=CYLINDRICAL_SURFACE('',#14648,0.199999999999999);
#12059=ADVANCED_FACE('',(#2334,#1357),#1706,.F.);
#12060=ADVANCED_FACE('',(#2335),#11493,.T.);
#12061=ADVANCED_FACE('',(#2336),#1707,.T.);
#12062=ADVANCED_FACE('',(#2337),#11494,.T.);
#12063=ADVANCED_FACE('',(#2338),#1708,.F.);
#12454=CLOSED_SHELL('',(#12059,#12060,#12061,#12062,#12063));
#14641=AXIS2_PLACEMENT_3D('',#21636,#17778,#17779);
#14642=AXIS2_PLACEMENT_3D('',#21637,#17780,#17781);
#14643=AXIS2_PLACEMENT_3D('',#21639,#17782,#17783);
#14644=AXIS2_PLACEMENT_3D('',#21641,#17784,#17785);
#14645=AXIS2_PLACEMENT_3D('',#21642,#17786,#17787);
#14646=AXIS2_PLACEMENT_3D('',#21644,#17788,#17789);
#14647=AXIS2_PLACEMENT_3D('',#21646,#17791,#17792);
#14648=AXIS2_PLACEMENT_3D('',#21647,#17793,#17794);
#14649=AXIS2_PLACEMENT_3D('',#21650,#17796,#17797);
#14650=AXIS2_PLACEMENT_3D('',#21651,#17798,#17799);
#17778=DIRECTION('axis',(0.,0.,1.));
#17779=DIRECTION('refdir',(1.,0.,0.));
#17780=DIRECTION('center_axis',(0.,1.,0.));
#17781=DIRECTION('ref_axis',(1.,0.,0.));
#17782=DIRECTION('center_axis',(0.,1.,0.));
#17783=DIRECTION('ref_axis',(1.,0.,0.));
#17784=DIRECTION('center_axis',(0.,1.,0.));
#17785=DIRECTION('ref_axis',(1.,0.,0.));
#17786=DIRECTION('center_axis',(0.,1.,0.));
#17787=DIRECTION('ref_axis',(1.,0.,0.));
#17788=DIRECTION('center_axis',(0.,1.,0.));
#17789=DIRECTION('ref_axis',(1.,0.,0.));
#17790=DIRECTION('',(0.,-1.,0.));
#17791=DIRECTION('center_axis',(0.,1.,0.));
#17792=DIRECTION('ref_axis',(1.,0.,0.));
#17793=DIRECTION('center_axis',(0.,1.,0.));
#17794=DIRECTION('ref_axis',(1.,0.,0.));
#17795=DIRECTION('',(0.,-1.,0.));
#17796=DIRECTION('center_axis',(0.,1.,0.));
#17797=DIRECTION('ref_axis',(1.,0.,0.));
#17798=DIRECTION('center_axis',(0.,1.,0.));
#17799=DIRECTION('ref_axis',(1.,0.,0.));
#21636=CARTESIAN_POINT('',(0.,0.,0.));
#21637=CARTESIAN_POINT('Origin',(19.3081475451951,0.8,13.6918524548049));
#21638=CARTESIAN_POINT('',(18.9581475451951,0.8,13.6918524548049));
#21639=CARTESIAN_POINT('Origin',(19.3081475451951,0.8,13.6918524548049));
#21640=CARTESIAN_POINT('',(19.1081475451951,0.8,13.6918524548049));
#21641=CARTESIAN_POINT('Origin',(19.3081475451951,0.8,13.6918524548049));
#21642=CARTESIAN_POINT('Origin',(19.3081475451951,0.8,13.6918524548049));
#21643=CARTESIAN_POINT('',(18.9581475451951,1.2,13.6918524548049));
#21644=CARTESIAN_POINT('Origin',(19.3081475451951,1.2,13.6918524548049));
#21645=CARTESIAN_POINT('',(18.9581475451951,0.8,13.6918524548049));
#21646=CARTESIAN_POINT('Origin',(19.3081475451951,1.2,13.6918524548049));
#21647=CARTESIAN_POINT('Origin',(19.3081475451951,0.1,13.6918524548049));
#21648=CARTESIAN_POINT('',(19.1081475451951,0.1,13.6918524548049));
#21649=CARTESIAN_POINT('',(19.1081475451951,0.1,13.6918524548049));
#21650=CARTESIAN_POINT('Origin',(19.3081475451951,0.1,13.6918524548049));
#21651=CARTESIAN_POINT('Origin',(19.3081475451951,0.1,13.6918524548049));
#23560=UNCERTAINTY_MEASURE_WITH_UNIT(LENGTH_MEASURE(0.001),#23729,
'DISTANCE_ACCURACY_VALUE',
'Maximum model space distance between geometric entities at asserted c
onnectivities');
#23611=UNCERTAINTY_MEASURE_WITH_UNIT(LENGTH_MEASURE(0.001),#23729,
'DISTANCE_ACCURACY_VALUE',
'Maximum model space distance between geometric entities at asserted c
onnectivities');
#23677=(
GEOMETRIC_REPRESENTATION_CONTEXT(3)
GLOBAL_UNCERTAINTY_ASSIGNED_CONTEXT((#23560))
GLOBAL_UNIT_ASSIGNED_CONTEXT((#23729,#23731,#23732))
REPRESENTATION_CONTEXT('','3D')
);
#23728=(
GEOMETRIC_REPRESENTATION_CONTEXT(3)
GLOBAL_UNCERTAINTY_ASSIGNED_CONTEXT((#23611))
GLOBAL_UNIT_ASSIGNED_CONTEXT((#23729,#23731,#23732))
REPRESENTATION_CONTEXT('','3D')
);
#23729=(
LENGTH_UNIT()
NAMED_UNIT(*)
SI_UNIT(.CENTI.,.METRE.)
);
#23731=(
NAMED_UNIT(*)
PLANE_ANGLE_UNIT()
SI_UNIT($,.RADIAN.)
);
#23732=(
NAMED_UNIT(*)
SI_UNIT($,.STERADIAN.)
SOLID_ANGLE_UNIT()
);
#23798=SHAPE_DEFINITION_REPRESENTATION(#23914,#24177);
#23914=PRODUCT_DEFINITION_SHAPE('',$,#24294);
#24177=SHAPE_REPRESENTATION('',(#14641),#23677);
#24228=PRODUCT_DEFINITION_CONTEXT('part definition',#24578,'design');
#24294=PRODUCT_DEFINITION('M4 short cap screw (23)',
'M4 short cap screw (23)',#24410,#24228);
#24410=PRODUCT_DEFINITION_FORMATION('',$,#24645);
#24578=APPLICATION_CONTEXT(
'Core Data for Automotive Mechanical Design Process');
#24579=PRODUCT_CONTEXT('part definition',#24578,'mechanical');
#24645=PRODUCT('M4 short cap screw (23)','M4 short cap screw (23)',
'M4 short cap screw (23)',(#24579));
#24766=COLOUR_RGB('Black',0.12,0.14,0.17);
#24767=FILL_AREA_STYLE_COLOUR('',#24766);
#24768=FILL_AREA_STYLE('',(#24767));
#24769=SURFACE_STYLE_FILL_AREA(#24768);
#24770=SURFACE_SIDE_STYLE('',(#24769));
#24771=SURFACE_STYLE_USAGE(.BOTH.,#24770);
#24772=PRESENTATION_STYLE_ASSIGNMENT((#24771));
ENDSEC;
END-ISO-10303-21;
